ISO-10303-21;
HEADER;
/* Generated by software containing ST-Developer
 * from STEP Tools, Inc. (www.steptools.com) 
 */

FILE_DESCRIPTION(
/* description */ (''),
/* implementation_level */ '2;1');

FILE_NAME(
/* name */ 'Ball_Screw_02.step',
/* time_stamp */ '2026-10-23T17:00:58+06:00',
/* author */ (''),
/* organization */ (''),
/* preprocessor_version */ 'ST-DEVELOPER v20.2',
/* originating_system */ 'Autodesk Translation Framework v15.15.0.0',
/* authorisation */ '');

FILE_SCHEMA (('AUTOMOTIVE_DESIGN { 1 0 10303 214 3 1 1 }'));
ENDSEC;

DATA;
#10=MECHANICAL_DESIGN_GEOMETRIC_PRESENTATION_REPRESENTATION('',(#112),#11385);
#67=SPHERICAL_SURFACE('',#6015,3.);
#75=TOROIDAL_SURFACE('',#6018,2.65761552865316,0.5);
#86=SHAPE_REPRESENTATION_RELATIONSHIP('SRR','None',#11438,#99);
#99=ADVANCED_BREP_SHAPE_REPRESENTATION('',(#125),#11378);
#112=STYLED_ITEM('',(#11574),#125);
#125=MANIFOLD_SOLID_BREP('Ball_Screw_02',#5348);
#166=FACE_BOUND('',#1249,.T.);
#167=FACE_BOUND('',#1259,.T.);
#267=CONICAL_SURFACE('',#6032,2.90761552865316,0.785398163397448);
#501=CIRCLE('',#6016,2.59807621135332);
#502=CIRCLE('',#6017,3.);
#503=CIRCLE('',#6019,2.65761552865316);
#504=CIRCLE('',#6020,0.5);
#505=CIRCLE('',#6021,3.15761552865316);
#506=CIRCLE('',#6023,3.15761552865316);
#507=CIRCLE('',#6033,2.65761552865316);
#600=CYLINDRICAL_SURFACE('',#6022,3.15761552865316);
#885=FACE_OUTER_BOUND('',#1245,.T.);
#886=FACE_OUTER_BOUND('',#1246,.T.);
#887=FACE_OUTER_BOUND('',#1247,.T.);
#888=FACE_OUTER_BOUND('',#1248,.T.);
#889=FACE_OUTER_BOUND('',#1250,.T.);
#890=FACE_OUTER_BOUND('',#1251,.T.);
#891=FACE_OUTER_BOUND('',#1252,.T.);
#892=FACE_OUTER_BOUND('',#1253,.T.);
#893=FACE_OUTER_BOUND('',#1254,.T.);
#894=FACE_OUTER_BOUND('',#1255,.T.);
#895=FACE_OUTER_BOUND('',#1256,.T.);
#896=FACE_OUTER_BOUND('',#1257,.T.);
#897=FACE_OUTER_BOUND('',#1258,.T.);
#1245=EDGE_LOOP('',(#4694,#4695,#4696));
#1246=EDGE_LOOP('',(#4697,#4698,#4699,#4700));
#1247=EDGE_LOOP('',(#4701,#4702,#4703,#4704));
#1248=EDGE_LOOP('',(#4705));
#1249=EDGE_LOOP('',(#4706));
#1250=EDGE_LOOP('',(#4707,#4708,#4709,#4710));
#1251=EDGE_LOOP('',(#4711,#4712,#4713,#4714));
#1252=EDGE_LOOP('',(#4715,#4716,#4717,#4718));
#1253=EDGE_LOOP('',(#4719,#4720,#4721,#4722));
#1254=EDGE_LOOP('',(#4723,#4724,#4725,#4726));
#1255=EDGE_LOOP('',(#4727,#4728,#4729,#4730));
#1256=EDGE_LOOP('',(#4731,#4732,#4733,#4734,#4735,#4736));
#1257=EDGE_LOOP('',(#4737,#4738,#4739,#4740));
#1258=EDGE_LOOP('',(#4741));
#1259=EDGE_LOOP('',(#4742,#4743,#4744,#4745,#4746,#4747));
#1713=LINE('',#9671,#2175);
#1714=LINE('',#9677,#2176);
#1715=LINE('',#9679,#2177);
#1716=LINE('',#9681,#2178);
#1717=LINE('',#9682,#2179);
#1718=LINE('',#9685,#2180);
#1719=LINE('',#9687,#2181);
#1720=LINE('',#9688,#2182);
#1721=LINE('',#9691,#2183);
#1722=LINE('',#9693,#2184);
#1723=LINE('',#9694,#2185);
#1724=LINE('',#9697,#2186);
#1725=LINE('',#9699,#2187);
#1726=LINE('',#9700,#2188);
#1727=LINE('',#9703,#2189);
#1728=LINE('',#9705,#2190);
#1729=LINE('',#9706,#2191);
#1730=LINE('',#9708,#2192);
#1731=LINE('',#9709,#2193);
#1732=LINE('',#9714,#2194);
#2175=VECTOR('',#7574,3.15761552865316);
#2176=VECTOR('',#7581,10.);
#2177=VECTOR('',#7582,10.);
#2178=VECTOR('',#7583,10.);
#2179=VECTOR('',#7584,10.);
#2180=VECTOR('',#7587,10.);
#2181=VECTOR('',#7588,10.);
#2182=VECTOR('',#7589,10.);
#2183=VECTOR('',#7592,10.);
#2184=VECTOR('',#7593,10.);
#2185=VECTOR('',#7594,10.);
#2186=VECTOR('',#7597,10.);
#2187=VECTOR('',#7598,10.);
#2188=VECTOR('',#7599,10.);
#2189=VECTOR('',#7602,10.);
#2190=VECTOR('',#7603,10.);
#2191=VECTOR('',#7604,10.);
#2192=VECTOR('',#7607,10.);
#2193=VECTOR('',#7608,10.);
#2194=VECTOR('',#7615,2.90761552865316);
#2608=VERTEX_POINT('',#9659);
#2609=VERTEX_POINT('',#9661);
#2610=VERTEX_POINT('',#9664);
#2611=VERTEX_POINT('',#9666);
#2612=VERTEX_POINT('',#9670);
#2613=VERTEX_POINT('',#9675);
#2614=VERTEX_POINT('',#9676);
#2615=VERTEX_POINT('',#9678);
#2616=VERTEX_POINT('',#9680);
#2617=VERTEX_POINT('',#9684);
#2618=VERTEX_POINT('',#9686);
#2619=VERTEX_POINT('',#9690);
#2620=VERTEX_POINT('',#9692);
#2621=VERTEX_POINT('',#9696);
#2622=VERTEX_POINT('',#9698);
#2623=VERTEX_POINT('',#9702);
#2624=VERTEX_POINT('',#9704);
#2625=VERTEX_POINT('',#9712);
#3312=EDGE_CURVE('',#2608,#2608,#501,.T.);
#3313=EDGE_CURVE('',#2609,#2608,#502,.T.);
#3314=EDGE_CURVE('',#2610,#2610,#503,.T.);
#3315=EDGE_CURVE('',#2610,#2611,#504,.T.);
#3316=EDGE_CURVE('',#2611,#2611,#505,.T.);
#3317=EDGE_CURVE('',#2611,#2612,#1713,.T.);
#3318=EDGE_CURVE('',#2612,#2612,#506,.T.);
#3319=EDGE_CURVE('',#2613,#2614,#1714,.T.);
#3320=EDGE_CURVE('',#2613,#2615,#1715,.T.);
#3321=EDGE_CURVE('',#2615,#2616,#1716,.T.);
#3322=EDGE_CURVE('',#2614,#2616,#1717,.T.);
#3323=EDGE_CURVE('',#2617,#2613,#1718,.T.);
#3324=EDGE_CURVE('',#2617,#2618,#1719,.T.);
#3325=EDGE_CURVE('',#2618,#2615,#1720,.T.);
#3326=EDGE_CURVE('',#2619,#2617,#1721,.T.);
#3327=EDGE_CURVE('',#2619,#2620,#1722,.T.);
#3328=EDGE_CURVE('',#2620,#2618,#1723,.T.);
#3329=EDGE_CURVE('',#2621,#2619,#1724,.T.);
#3330=EDGE_CURVE('',#2621,#2622,#1725,.T.);
#3331=EDGE_CURVE('',#2622,#2620,#1726,.T.);
#3332=EDGE_CURVE('',#2623,#2621,#1727,.T.);
#3333=EDGE_CURVE('',#2623,#2624,#1728,.T.);
#3334=EDGE_CURVE('',#2624,#2622,#1729,.T.);
#3335=EDGE_CURVE('',#2614,#2623,#1730,.T.);
#3336=EDGE_CURVE('',#2616,#2624,#1731,.T.);
#3337=EDGE_CURVE('',#2625,#2625,#507,.T.);
#3338=EDGE_CURVE('',#2625,#2612,#1732,.T.);
#4694=ORIENTED_EDGE('',*,*,#3312,.F.);
#4695=ORIENTED_EDGE('',*,*,#3313,.F.);
#4696=ORIENTED_EDGE('',*,*,#3313,.T.);
#4697=ORIENTED_EDGE('',*,*,#3314,.T.);
#4698=ORIENTED_EDGE('',*,*,#3315,.T.);
#4699=ORIENTED_EDGE('',*,*,#3316,.T.);
#4700=ORIENTED_EDGE('',*,*,#3315,.F.);
#4701=ORIENTED_EDGE('',*,*,#3316,.F.);
#4702=ORIENTED_EDGE('',*,*,#3317,.T.);
#4703=ORIENTED_EDGE('',*,*,#3318,.F.);
#4704=ORIENTED_EDGE('',*,*,#3317,.F.);
#4705=ORIENTED_EDGE('',*,*,#3314,.F.);
#4706=ORIENTED_EDGE('',*,*,#3312,.T.);
#4707=ORIENTED_EDGE('',*,*,#3319,.F.);
#4708=ORIENTED_EDGE('',*,*,#3320,.T.);
#4709=ORIENTED_EDGE('',*,*,#3321,.T.);
#4710=ORIENTED_EDGE('',*,*,#3322,.F.);
#4711=ORIENTED_EDGE('',*,*,#3323,.F.);
#4712=ORIENTED_EDGE('',*,*,#3324,.T.);
#4713=ORIENTED_EDGE('',*,*,#3325,.T.);
#4714=ORIENTED_EDGE('',*,*,#3320,.F.);
#4715=ORIENTED_EDGE('',*,*,#3326,.F.);
#4716=ORIENTED_EDGE('',*,*,#3327,.T.);
#4717=ORIENTED_EDGE('',*,*,#3328,.T.);
#4718=ORIENTED_EDGE('',*,*,#3324,.F.);
#4719=ORIENTED_EDGE('',*,*,#3329,.F.);
#4720=ORIENTED_EDGE('',*,*,#3330,.T.);
#4721=ORIENTED_EDGE('',*,*,#3331,.T.);
#4722=ORIENTED_EDGE('',*,*,#3327,.F.);
#4723=ORIENTED_EDGE('',*,*,#3332,.F.);
#4724=ORIENTED_EDGE('',*,*,#3333,.T.);
#4725=ORIENTED_EDGE('',*,*,#3334,.T.);
#4726=ORIENTED_EDGE('',*,*,#3330,.F.);
#4727=ORIENTED_EDGE('',*,*,#3335,.F.);
#4728=ORIENTED_EDGE('',*,*,#3322,.T.);
#4729=ORIENTED_EDGE('',*,*,#3336,.T.);
#4730=ORIENTED_EDGE('',*,*,#3333,.F.);
#4731=ORIENTED_EDGE('',*,*,#3336,.F.);
#4732=ORIENTED_EDGE('',*,*,#3321,.F.);
#4733=ORIENTED_EDGE('',*,*,#3325,.F.);
#4734=ORIENTED_EDGE('',*,*,#3328,.F.);
#4735=ORIENTED_EDGE('',*,*,#3331,.F.);
#4736=ORIENTED_EDGE('',*,*,#3334,.F.);
#4737=ORIENTED_EDGE('',*,*,#3337,.T.);
#4738=ORIENTED_EDGE('',*,*,#3338,.T.);
#4739=ORIENTED_EDGE('',*,*,#3318,.T.);
#4740=ORIENTED_EDGE('',*,*,#3338,.F.);
#4741=ORIENTED_EDGE('',*,*,#3337,.F.);
#4742=ORIENTED_EDGE('',*,*,#3319,.T.);
#4743=ORIENTED_EDGE('',*,*,#3335,.T.);
#4744=ORIENTED_EDGE('',*,*,#3332,.T.);
#4745=ORIENTED_EDGE('',*,*,#3329,.T.);
#4746=ORIENTED_EDGE('',*,*,#3326,.T.);
#4747=ORIENTED_EDGE('',*,*,#3323,.T.);
#4991=PLANE('',#6024);
#4992=PLANE('',#6025);
#4993=PLANE('',#6026);
#4994=PLANE('',#6027);
#4995=PLANE('',#6028);
#4996=PLANE('',#6029);
#4997=PLANE('',#6030);
#4998=PLANE('',#6031);
#4999=PLANE('',#6034);
#5297=ADVANCED_FACE('',(#885),#67,.T.);
#5298=ADVANCED_FACE('',(#886),#75,.T.);
#5299=ADVANCED_FACE('',(#887),#600,.T.);
#5300=ADVANCED_FACE('',(#888,#166),#4991,.F.);
#5301=ADVANCED_FACE('',(#889),#4992,.F.);
#5302=ADVANCED_FACE('',(#890),#4993,.F.);
#5303=ADVANCED_FACE('',(#891),#4994,.F.);
#5304=ADVANCED_FACE('',(#892),#4995,.F.);
#5305=ADVANCED_FACE('',(#893),#4996,.F.);
#5306=ADVANCED_FACE('',(#894),#4997,.F.);
#5307=ADVANCED_FACE('',(#895),#4998,.F.);
#5308=ADVANCED_FACE('',(#896),#267,.T.);
#5309=ADVANCED_FACE('',(#897,#167),#4999,.T.);
#5348=CLOSED_SHELL('',(#5297,#5298,#5299,#5300,#5301,#5302,#5303,#5304,
#5305,#5306,#5307,#5308,#5309));
#6014=AXIS2_PLACEMENT_3D('',#9657,#7556,#7557);
#6015=AXIS2_PLACEMENT_3D('',#9658,#7558,#7559);
#6016=AXIS2_PLACEMENT_3D('',#9660,#7560,#7561);
#6017=AXIS2_PLACEMENT_3D('',#9662,#7562,#7563);
#6018=AXIS2_PLACEMENT_3D('',#9663,#7564,#7565);
#6019=AXIS2_PLACEMENT_3D('',#9665,#7566,#7567);
#6020=AXIS2_PLACEMENT_3D('',#9667,#7568,#7569);
#6021=AXIS2_PLACEMENT_3D('',#9668,#7570,#7571);
#6022=AXIS2_PLACEMENT_3D('',#9669,#7572,#7573);
#6023=AXIS2_PLACEMENT_3D('',#9672,#7575,#7576);
#6024=AXIS2_PLACEMENT_3D('',#9673,#7577,#7578);
#6025=AXIS2_PLACEMENT_3D('',#9674,#7579,#7580);
#6026=AXIS2_PLACEMENT_3D('',#9683,#7585,#7586);
#6027=AXIS2_PLACEMENT_3D('',#9689,#7590,#7591);
#6028=AXIS2_PLACEMENT_3D('',#9695,#7595,#7596);
#6029=AXIS2_PLACEMENT_3D('',#9701,#7600,#7601);
#6030=AXIS2_PLACEMENT_3D('',#9707,#7605,#7606);
#6031=AXIS2_PLACEMENT_3D('',#9710,#7609,#7610);
#6032=AXIS2_PLACEMENT_3D('',#9711,#7611,#7612);
#6033=AXIS2_PLACEMENT_3D('',#9713,#7613,#7614);
#6034=AXIS2_PLACEMENT_3D('',#9715,#7616,#7617);
#7556=DIRECTION('axis',(0.,0.,1.));
#7557=DIRECTION('refdir',(1.,0.,0.));
#7558=DIRECTION('center_axis',(0.,0.,-1.));
#7559=DIRECTION('ref_axis',(1.,0.,0.));
#7560=DIRECTION('center_axis',(0.,-1.22464679914735E-16,1.));
#7561=DIRECTION('ref_axis',(0.,-1.,-1.22464679914735E-16));
#7562=DIRECTION('center_axis',(0.,1.,1.22464679914735E-16));
#7563=DIRECTION('ref_axis',(-1.,0.,0.));
#7564=DIRECTION('center_axis',(0.,1.22464679914735E-16,-1.));
#7565=DIRECTION('ref_axis',(1.,0.,0.));
#7566=DIRECTION('center_axis',(0.,-1.22464679914735E-16,1.));
#7567=DIRECTION('ref_axis',(1.,0.,0.));
#7568=DIRECTION('center_axis',(0.,1.,1.22464679914735E-16));
#7569=DIRECTION('ref_axis',(-1.,0.,0.));
#7570=DIRECTION('center_axis',(0.,1.22464679914735E-16,-1.));
#7571=DIRECTION('ref_axis',(1.,0.,0.));
#7572=DIRECTION('center_axis',(0.,1.22464679914735E-16,-1.));
#7573=DIRECTION('ref_axis',(1.,0.,0.));
#7574=DIRECTION('',(0.,-1.22464679914735E-16,1.));
#7575=DIRECTION('center_axis',(0.,-1.22464679914735E-16,1.));
#7576=DIRECTION('ref_axis',(1.,0.,0.));
#7577=DIRECTION('center_axis',(0.,-1.22464679914735E-16,1.));
#7578=DIRECTION('ref_axis',(1.,0.,0.));
#7579=DIRECTION('center_axis',(-0.5,-0.866025403784439,-1.06057523872491E-16));
#7580=DIRECTION('ref_axis',(-0.866025403784439,0.5,6.12323399573677E-17));
#7581=DIRECTION('',(-0.866025403784439,0.5,6.12323399573677E-17));
#7582=DIRECTION('',(0.,1.22464679914735E-16,-1.));
#7583=DIRECTION('',(-0.866025403784439,0.5,6.12323399573677E-17));
#7584=DIRECTION('',(0.,1.22464679914735E-16,-1.));
#7585=DIRECTION('center_axis',(0.5,-0.866025403784439,-1.06057523872491E-16));
#7586=DIRECTION('ref_axis',(-0.866025403784439,-0.5,-6.12323399573677E-17));
#7587=DIRECTION('',(-0.866025403784439,-0.5,-6.12323399573677E-17));
#7588=DIRECTION('',(0.,1.22464679914735E-16,-1.));
#7589=DIRECTION('',(-0.866025403784439,-0.5,-6.12323399573677E-17));
#7590=DIRECTION('center_axis',(1.,0.,0.));
#7591=DIRECTION('ref_axis',(0.,-1.,-1.22464679914735E-16));
#7592=DIRECTION('',(0.,-1.,-1.22464679914735E-16));
#7593=DIRECTION('',(0.,1.22464679914735E-16,-1.));
#7594=DIRECTION('',(0.,-1.,-1.22464679914735E-16));
#7595=DIRECTION('center_axis',(0.5,0.866025403784439,1.06057523872491E-16));
#7596=DIRECTION('ref_axis',(0.866025403784439,-0.5,-6.12323399573677E-17));
#7597=DIRECTION('',(0.866025403784439,-0.5,-6.12323399573677E-17));
#7598=DIRECTION('',(0.,1.22464679914735E-16,-1.));
#7599=DIRECTION('',(0.866025403784439,-0.5,-6.12323399573677E-17));
#7600=DIRECTION('center_axis',(-0.5,0.866025403784439,1.06057523872491E-16));
#7601=DIRECTION('ref_axis',(0.866025403784439,0.5,6.12323399573676E-17));
#7602=DIRECTION('',(0.866025403784439,0.5,6.12323399573676E-17));
#7603=DIRECTION('',(0.,1.22464679914735E-16,-1.));
#7604=DIRECTION('',(0.866025403784439,0.5,6.12323399573676E-17));
#7605=DIRECTION('center_axis',(-1.,6.40987562127855E-16,7.84983366253143E-32));
#7606=DIRECTION('ref_axis',(6.40987562127855E-16,1.,1.22464679914735E-16));
#7607=DIRECTION('',(6.40987562127855E-16,1.,1.22464679914735E-16));
#7608=DIRECTION('',(6.40987562127855E-16,1.,1.22464679914735E-16));
#7609=DIRECTION('center_axis',(0.,1.22464679914735E-16,-1.));
#7610=DIRECTION('ref_axis',(1.,0.,0.));
#7611=DIRECTION('center_axis',(0.,1.22464679914735E-16,-1.));
#7612=DIRECTION('ref_axis',(1.,0.,0.));
#7613=DIRECTION('center_axis',(0.,1.22464679914735E-16,-1.));
#7614=DIRECTION('ref_axis',(1.,0.,0.));
#7615=DIRECTION('',(-0.707106781186547,2.11959791839945E-32,-0.707106781186548));
#7616=DIRECTION('center_axis',(0.,-1.22464679914735E-16,1.));
#7617=DIRECTION('ref_axis',(1.,0.,0.));
#9657=CARTESIAN_POINT('',(0.,0.,0.));
#9658=CARTESIAN_POINT('Origin',(-4.88927830720691,5.31072169279307,9.2));
#9659=CARTESIAN_POINT('',(-7.48735451856022,5.31072169279307,7.7));
#9660=CARTESIAN_POINT('Origin',(-4.88927830720691,5.31072169279307,7.7));
#9661=CARTESIAN_POINT('',(-4.88927830720691,5.31072169279307,6.2));
#9662=CARTESIAN_POINT('Origin',(-4.88927830720691,5.31072169279307,9.2));
#9663=CARTESIAN_POINT('Origin',(-4.88927830720691,5.31072169279307,8.2));
#9664=CARTESIAN_POINT('',(-7.54689383586007,5.31072169279307,7.7));
#9665=CARTESIAN_POINT('Origin',(-4.88927830720691,5.31072169279307,7.7));
#9666=CARTESIAN_POINT('',(-8.04689383586007,5.31072169279307,8.2));
#9667=CARTESIAN_POINT('Origin',(-7.54689383586007,5.31072169279307,8.2));
#9668=CARTESIAN_POINT('Origin',(-4.88927830720691,5.31072169279307,8.2));
#9669=CARTESIAN_POINT('Origin',(-4.88927830720691,5.31072169279308,19.));
#9670=CARTESIAN_POINT('',(-8.04689383586007,5.31072169279308,18.5));
#9671=CARTESIAN_POINT('',(-8.04689383586007,5.31072169279308,19.));
#9672=CARTESIAN_POINT('Origin',(-4.88927830720691,5.31072169279308,18.5));
#9673=CARTESIAN_POINT('Origin',(-4.88927830720691,5.31072169279307,7.7));
#9674=CARTESIAN_POINT('Origin',(-4.88927830720691,3.5786708852242,19.));
#9675=CARTESIAN_POINT('',(-4.88927830720691,3.5786708852242,19.));
#9676=CARTESIAN_POINT('',(-6.38927830720691,4.44469628900864,19.));
#9677=CARTESIAN_POINT('',(-5.26427830720691,3.79517723617031,19.));
#9678=CARTESIAN_POINT('',(-4.88927830720691,3.5786708852242,18.));
#9679=CARTESIAN_POINT('',(-4.88927830720691,3.5786708852242,19.));
#9680=CARTESIAN_POINT('',(-6.38927830720691,4.44469628900864,18.));
#9681=CARTESIAN_POINT('',(-6.38927830720691,4.44469628900864,18.));
#9682=CARTESIAN_POINT('',(-6.38927830720691,4.44469628900864,19.));
#9683=CARTESIAN_POINT('Origin',(-3.38927830720691,4.44469628900864,19.));
#9684=CARTESIAN_POINT('',(-3.38927830720691,4.44469628900864,19.));
#9685=CARTESIAN_POINT('',(-3.76427830720691,4.22818993806253,19.));
#9686=CARTESIAN_POINT('',(-3.38927830720691,4.44469628900864,18.));
#9687=CARTESIAN_POINT('',(-3.38927830720691,4.44469628900864,19.));
#9688=CARTESIAN_POINT('',(-4.88927830720691,3.5786708852242,18.));
#9689=CARTESIAN_POINT('Origin',(-3.38927830720691,6.17674709657752,19.));
#9690=CARTESIAN_POINT('',(-3.38927830720691,6.17674709657752,19.));
#9691=CARTESIAN_POINT('',(-3.38927830720691,5.7437343946853,19.));
#9692=CARTESIAN_POINT('',(-3.38927830720691,6.17674709657751,18.));
#9693=CARTESIAN_POINT('',(-3.38927830720691,6.17674709657752,19.));
#9694=CARTESIAN_POINT('',(-3.38927830720691,4.44469628900864,18.));
#9695=CARTESIAN_POINT('Origin',(-4.88927830720691,7.04277250036196,19.));
#9696=CARTESIAN_POINT('',(-4.88927830720691,7.04277250036196,19.));
#9697=CARTESIAN_POINT('',(-4.51427830720691,6.82626614941585,19.));
#9698=CARTESIAN_POINT('',(-4.88927830720691,7.04277250036195,18.));
#9699=CARTESIAN_POINT('',(-4.88927830720691,7.04277250036196,19.));
#9700=CARTESIAN_POINT('',(-3.38927830720691,6.17674709657751,18.));
#9701=CARTESIAN_POINT('Origin',(-6.38927830720691,6.17674709657752,19.));
#9702=CARTESIAN_POINT('',(-6.38927830720691,6.17674709657752,19.));
#9703=CARTESIAN_POINT('',(-6.01427830720691,6.39325344752363,19.));
#9704=CARTESIAN_POINT('',(-6.38927830720691,6.17674709657751,18.));
#9705=CARTESIAN_POINT('',(-6.38927830720691,6.17674709657752,19.));
#9706=CARTESIAN_POINT('',(-4.88927830720691,7.04277250036195,18.));
#9707=CARTESIAN_POINT('Origin',(-6.38927830720691,4.44469628900864,19.));
#9708=CARTESIAN_POINT('',(-6.38927830720691,4.87770899090086,19.));
#9709=CARTESIAN_POINT('',(-6.38927830720691,6.17674709657751,18.));
#9710=CARTESIAN_POINT('Origin',(-4.88927830720691,5.31072169279307,18.));
#9711=CARTESIAN_POINT('Origin',(-4.88927830720691,5.31072169279308,18.75));
#9712=CARTESIAN_POINT('',(-7.54689383586007,5.31072169279308,19.));
#9713=CARTESIAN_POINT('Origin',(-4.88927830720691,5.31072169279308,19.));
#9714=CARTESIAN_POINT('',(-7.79689383586007,5.31072169279308,18.75));
#9715=CARTESIAN_POINT('Origin',(-4.88927830720691,5.31072169279308,19.));
#11363=UNCERTAINTY_MEASURE_WITH_UNIT(LENGTH_MEASURE(0.01),#11386,
'DISTANCE_ACCURACY_VALUE',
'Maximum model space distance between geometric entities at asserted c
onnectivities');
#11370=UNCERTAINTY_MEASURE_WITH_UNIT(LENGTH_MEASURE(0.01),#11386,
'DISTANCE_ACCURACY_VALUE',
'Maximum model space distance between geometric entities at asserted c
onnectivities');
#11378=(
GEOMETRIC_REPRESENTATION_CONTEXT(3)
GLOBAL_UNCERTAINTY_ASSIGNED_CONTEXT((#11363))
GLOBAL_UNIT_ASSIGNED_CONTEXT((#11386,#11388,#11389))
REPRESENTATION_CONTEXT('','3D')
);
#11385=(
GEOMETRIC_REPRESENTATION_CONTEXT(3)
GLOBAL_UNCERTAINTY_ASSIGNED_CONTEXT((#11370))
GLOBAL_UNIT_ASSIGNED_CONTEXT((#11386,#11388,#11389))
REPRESENTATION_CONTEXT('','3D')
);
#11386=(
LENGTH_UNIT()
NAMED_UNIT(*)
SI_UNIT(.MILLI.,.METRE.)
);
#11388=(
NAMED_UNIT(*)
PLANE_ANGLE_UNIT()
SI_UNIT($,.RADIAN.)
);
#11389=(
NAMED_UNIT(*)
SI_UNIT($,.STERADIAN.)
SOLID_ANGLE_UNIT()
);
#11397=SHAPE_DEFINITION_REPRESENTATION(#11411,#11438);
#11411=PRODUCT_DEFINITION_SHAPE('',$,#11453);
#11438=SHAPE_REPRESENTATION('',(#6014),#11378);
#11445=PRODUCT_DEFINITION_CONTEXT('part definition',#11489,'design');
#11453=PRODUCT_DEFINITION('Ball_Screw_02','Ball_Screw_02',#11467,#11445);
#11467=PRODUCT_DEFINITION_FORMATION('',$,#11498);
#11489=APPLICATION_CONTEXT(
'Core Data for Automotive Mechanical Design Process');
#11490=PRODUCT_CONTEXT('part definition',#11489,'mechanical');
#11498=PRODUCT('Ball_Screw_02','Ball_Screw_02',$,(#11490));
#11568=COLOUR_RGB('Black',0.12,0.14,0.17);
#11569=FILL_AREA_STYLE_COLOUR('',#11568);
#11570=FILL_AREA_STYLE('',(#11569));
#11571=SURFACE_STYLE_FILL_AREA(#11570);
#11572=SURFACE_SIDE_STYLE('',(#11571));
#11573=SURFACE_STYLE_USAGE(.BOTH.,#11572);
#11574=PRESENTATION_STYLE_ASSIGNMENT((#11573));
ENDSEC;
END-ISO-10303-21;
